ISO-10303-21;
HEADER;
/* Generated by software containing ST-Developer
 * from STEP Tools, Inc. (www.steptools.com) 
 */

FILE_DESCRIPTION(
/* description */ ('PAT-015'),
/* implementation_level */ '2;1');

FILE_NAME(
/* name */ 'Upper diaphragm plate.step',
/* time_stamp */ '2026-10-29T16:03:43-07:00',
/* author */ (''),
/* organization */ (''),
/* preprocessor_version */ 'ST-DEVELOPER v20.2',
/* originating_system */ 'Autodesk Translation Framework v15.17.0.0',
/* authorisation */ '');

FILE_SCHEMA (('AUTOMOTIVE_DESIGN { 1 0 10303 214 3 1 1 }'));
ENDSEC;

DATA;
#10=MECHANICAL_DESIGN_GEOMETRIC_PRESENTATION_REPRESENTATION('',(#242),#10266);
#194=SHAPE_REPRESENTATION_RELATIONSHIP('SRR','None',#10365,#217);
#217=ADVANCED_BREP_SHAPE_REPRESENTATION('',(#267),#10253);
#242=STYLED_ITEM('',(#10540),#267);
#267=MANIFOLD_SOLID_BREP('Body1',#4701);
#386=FACE_BOUND('',#1113,.T.);
#387=FACE_BOUND('',#1115,.T.);
#388=FACE_BOUND('',#1119,.T.);
#389=FACE_BOUND('',#1121,.T.);
#499=PLANE('',#5296);
#500=PLANE('',#5297);
#501=PLANE('',#5304);
#502=PLANE('',#5305);
#733=FACE_OUTER_BOUND('',#1110,.T.);
#734=FACE_OUTER_BOUND('',#1111,.T.);
#735=FACE_OUTER_BOUND('',#1112,.T.);
#736=FACE_OUTER_BOUND('',#1114,.T.);
#737=FACE_OUTER_BOUND('',#1116,.T.);
#738=FACE_OUTER_BOUND('',#1117,.T.);
#739=FACE_OUTER_BOUND('',#1118,.T.);
#740=FACE_OUTER_BOUND('',#1120,.T.);
#1110=EDGE_LOOP('',(#3807,#3808,#3809,#3810));
#1111=EDGE_LOOP('',(#3811,#3812,#3813,#3814));
#1112=EDGE_LOOP('',(#3815));
#1113=EDGE_LOOP('',(#3816));
#1114=EDGE_LOOP('',(#3817));
#1115=EDGE_LOOP('',(#3818));
#1116=EDGE_LOOP('',(#3819,#3820,#3821,#3822));
#1117=EDGE_LOOP('',(#3823,#3824,#3825,#3826));
#1118=EDGE_LOOP('',(#3827));
#1119=EDGE_LOOP('',(#3828));
#1120=EDGE_LOOP('',(#3829));
#1121=EDGE_LOOP('',(#3830));
#1476=LINE('',#8800,#1756);
#1477=LINE('',#8806,#1757);
#1478=LINE('',#8816,#1758);
#1479=LINE('',#8820,#1759);
#1756=VECTOR('',#6353,0.41);
#1757=VECTOR('',#6360,0.6);
#1758=VECTOR('',#6373,0.16);
#1759=VECTOR('',#6378,2.2);
#2015=CIRCLE('',#5291,0.41);
#2016=CIRCLE('',#5292,0.41);
#2017=CIRCLE('',#5294,0.6);
#2018=CIRCLE('',#5295,0.6);
#2019=CIRCLE('',#5298,2.2);
#2020=CIRCLE('',#5300,0.16);
#2021=CIRCLE('',#5301,0.16);
#2022=CIRCLE('',#5303,2.2);
#2349=VERTEX_POINT('',#8797);
#2350=VERTEX_POINT('',#8799);
#2351=VERTEX_POINT('',#8803);
#2352=VERTEX_POINT('',#8805);
#2353=VERTEX_POINT('',#8810);
#2354=VERTEX_POINT('',#8813);
#2355=VERTEX_POINT('',#8815);
#2356=VERTEX_POINT('',#8819);
#2859=EDGE_CURVE('',#2349,#2349,#2015,.T.);
#2860=EDGE_CURVE('',#2349,#2350,#1476,.T.);
#2861=EDGE_CURVE('',#2350,#2350,#2016,.T.);
#2862=EDGE_CURVE('',#2351,#2351,#2017,.T.);
#2863=EDGE_CURVE('',#2351,#2352,#1477,.T.);
#2864=EDGE_CURVE('',#2352,#2352,#2018,.T.);
#2865=EDGE_CURVE('',#2353,#2353,#2019,.T.);
#2866=EDGE_CURVE('',#2354,#2354,#2020,.T.);
#2867=EDGE_CURVE('',#2354,#2355,#1478,.T.);
#2868=EDGE_CURVE('',#2355,#2355,#2021,.T.);
#2869=EDGE_CURVE('',#2353,#2356,#1479,.T.);
#2870=EDGE_CURVE('',#2356,#2356,#2022,.T.);
#3807=ORIENTED_EDGE('',*,*,#2859,.F.);
#3808=ORIENTED_EDGE('',*,*,#2860,.T.);
#3809=ORIENTED_EDGE('',*,*,#2861,.F.);
#3810=ORIENTED_EDGE('',*,*,#2860,.F.);
#3811=ORIENTED_EDGE('',*,*,#2862,.F.);
#3812=ORIENTED_EDGE('',*,*,#2863,.T.);
#3813=ORIENTED_EDGE('',*,*,#2864,.F.);
#3814=ORIENTED_EDGE('',*,*,#2863,.F.);
#3815=ORIENTED_EDGE('',*,*,#2862,.T.);
#3816=ORIENTED_EDGE('',*,*,#2859,.T.);
#3817=ORIENTED_EDGE('',*,*,#2865,.T.);
#3818=ORIENTED_EDGE('',*,*,#2864,.T.);
#3819=ORIENTED_EDGE('',*,*,#2866,.F.);
#3820=ORIENTED_EDGE('',*,*,#2867,.T.);
#3821=ORIENTED_EDGE('',*,*,#2868,.T.);
#3822=ORIENTED_EDGE('',*,*,#2867,.F.);
#3823=ORIENTED_EDGE('',*,*,#2865,.F.);
#3824=ORIENTED_EDGE('',*,*,#2869,.T.);
#3825=ORIENTED_EDGE('',*,*,#2870,.T.);
#3826=ORIENTED_EDGE('',*,*,#2869,.F.);
#3827=ORIENTED_EDGE('',*,*,#2861,.T.);
#3828=ORIENTED_EDGE('',*,*,#2866,.T.);
#3829=ORIENTED_EDGE('',*,*,#2870,.F.);
#3830=ORIENTED_EDGE('',*,*,#2868,.F.);
#4371=CYLINDRICAL_SURFACE('',#5290,0.41);
#4372=CYLINDRICAL_SURFACE('',#5293,0.6);
#4373=CYLINDRICAL_SURFACE('',#5299,0.16);
#4374=CYLINDRICAL_SURFACE('',#5302,2.2);
#4568=ADVANCED_FACE('',(#733),#4371,.F.);
#4569=ADVANCED_FACE('',(#734),#4372,.T.);
#4570=ADVANCED_FACE('',(#735,#386),#499,.T.);
#4571=ADVANCED_FACE('',(#736,#387),#500,.T.);
#4572=ADVANCED_FACE('',(#737),#4373,.F.);
#4573=ADVANCED_FACE('',(#738),#4374,.T.);
#4574=ADVANCED_FACE('',(#739,#388),#501,.T.);
#4575=ADVANCED_FACE('',(#740,#389),#502,.F.);
#4701=CLOSED_SHELL('',(#4568,#4569,#4570,#4571,#4572,#4573,#4574,#4575));
#5289=AXIS2_PLACEMENT_3D('',#8795,#6347,#6348);
#5290=AXIS2_PLACEMENT_3D('',#8796,#6349,#6350);
#5291=AXIS2_PLACEMENT_3D('',#8798,#6351,#6352);
#5292=AXIS2_PLACEMENT_3D('',#8801,#6354,#6355);
#5293=AXIS2_PLACEMENT_3D('',#8802,#6356,#6357);
#5294=AXIS2_PLACEMENT_3D('',#8804,#6358,#6359);
#5295=AXIS2_PLACEMENT_3D('',#8807,#6361,#6362);
#5296=AXIS2_PLACEMENT_3D('',#8808,#6363,#6364);
#5297=AXIS2_PLACEMENT_3D('',#8809,#6365,#6366);
#5298=AXIS2_PLACEMENT_3D('',#8811,#6367,#6368);
#5299=AXIS2_PLACEMENT_3D('',#8812,#6369,#6370);
#5300=AXIS2_PLACEMENT_3D('',#8814,#6371,#6372);
#5301=AXIS2_PLACEMENT_3D('',#8817,#6374,#6375);
#5302=AXIS2_PLACEMENT_3D('',#8818,#6376,#6377);
#5303=AXIS2_PLACEMENT_3D('',#8821,#6379,#6380);
#5304=AXIS2_PLACEMENT_3D('',#8822,#6381,#6382);
#5305=AXIS2_PLACEMENT_3D('',#8823,#6383,#6384);
#6347=DIRECTION('axis',(0.,0.,1.));
#6348=DIRECTION('refdir',(1.,0.,0.));
#6349=DIRECTION('center_axis',(0.,0.,1.));
#6350=DIRECTION('ref_axis',(1.,0.,0.));
#6351=DIRECTION('center_axis',(0.,0.,-1.));
#6352=DIRECTION('ref_axis',(1.,0.,0.));
#6353=DIRECTION('',(0.,0.,-1.));
#6354=DIRECTION('center_axis',(0.,0.,1.));
#6355=DIRECTION('ref_axis',(1.,0.,0.));
#6356=DIRECTION('center_axis',(0.,0.,1.));
#6357=DIRECTION('ref_axis',(1.,0.,0.));
#6358=DIRECTION('center_axis',(0.,0.,1.));
#6359=DIRECTION('ref_axis',(1.,0.,0.));
#6360=DIRECTION('',(0.,0.,-1.));
#6361=DIRECTION('center_axis',(0.,0.,-1.));
#6362=DIRECTION('ref_axis',(1.,0.,0.));
#6363=DIRECTION('center_axis',(0.,0.,1.));
#6364=DIRECTION('ref_axis',(1.,0.,0.));
#6365=DIRECTION('center_axis',(0.,0.,1.));
#6366=DIRECTION('ref_axis',(1.,0.,0.));
#6367=DIRECTION('center_axis',(0.,0.,1.));
#6368=DIRECTION('ref_axis',(1.,0.,0.));
#6369=DIRECTION('center_axis',(0.,0.,1.));
#6370=DIRECTION('ref_axis',(1.,0.,0.));
#6371=DIRECTION('center_axis',(0.,0.,-1.));
#6372=DIRECTION('ref_axis',(1.,0.,0.));
#6373=DIRECTION('',(0.,0.,-1.));
#6374=DIRECTION('center_axis',(0.,0.,-1.));
#6375=DIRECTION('ref_axis',(1.,0.,0.));
#6376=DIRECTION('center_axis',(0.,0.,1.));
#6377=DIRECTION('ref_axis',(1.,0.,0.));
#6378=DIRECTION('',(0.,0.,-1.));
#6379=DIRECTION('center_axis',(0.,0.,1.));
#6380=DIRECTION('ref_axis',(1.,0.,0.));
#6381=DIRECTION('center_axis',(0.,0.,1.));
#6382=DIRECTION('ref_axis',(1.,0.,0.));
#6383=DIRECTION('center_axis',(0.,0.,1.));
#6384=DIRECTION('ref_axis',(1.,0.,0.));
#8795=CARTESIAN_POINT('',(0.,0.,0.));
#8796=CARTESIAN_POINT('Origin',(0.,0.,5.3));
#8797=CARTESIAN_POINT('',(-0.41,-5.02105187650415E-17,5.7));
#8798=CARTESIAN_POINT('Origin',(0.,0.,5.7));
#8799=CARTESIAN_POINT('',(-0.41,-5.02105187650415E-17,5.3));
#8800=CARTESIAN_POINT('',(-0.41,-5.02105187650415E-17,5.3));
#8801=CARTESIAN_POINT('Origin',(0.,0.,5.3));
#8802=CARTESIAN_POINT('Origin',(0.,0.,5.3));
#8803=CARTESIAN_POINT('',(-0.6,-7.34788079488412E-17,5.7));
#8804=CARTESIAN_POINT('Origin',(0.,0.,5.7));
#8805=CARTESIAN_POINT('',(-0.6,-7.34788079488412E-17,5.3));
#8806=CARTESIAN_POINT('',(-0.6,-7.34788079488412E-17,5.3));
#8807=CARTESIAN_POINT('Origin',(0.,0.,5.3));
#8808=CARTESIAN_POINT('Origin',(0.,0.,5.7));
#8809=CARTESIAN_POINT('Origin',(0.,0.,5.3));
#8810=CARTESIAN_POINT('',(-2.2,-2.69422295812418E-16,5.3));
#8811=CARTESIAN_POINT('Origin',(0.,0.,5.3));
#8812=CARTESIAN_POINT('Origin',(0.,0.,5.1));
#8813=CARTESIAN_POINT('',(-0.16,-1.95943487863577E-17,5.3));
#8814=CARTESIAN_POINT('Origin',(0.,0.,5.3));
#8815=CARTESIAN_POINT('',(-0.16,-1.95943487863577E-17,5.1));
#8816=CARTESIAN_POINT('',(-0.16,-1.95943487863577E-17,5.1));
#8817=CARTESIAN_POINT('Origin',(0.,0.,5.1));
#8818=CARTESIAN_POINT('Origin',(0.,0.,5.1));
#8819=CARTESIAN_POINT('',(-2.2,-2.69422295812418E-16,5.1));
#8820=CARTESIAN_POINT('',(-2.2,-2.69422295812418E-16,5.1));
#8821=CARTESIAN_POINT('Origin',(0.,0.,5.1));
#8822=CARTESIAN_POINT('Origin',(0.,0.,5.3));
#8823=CARTESIAN_POINT('Origin',(0.,0.,5.1));
#10228=UNCERTAINTY_MEASURE_WITH_UNIT(LENGTH_MEASURE(0.001),#10267,
'DISTANCE_ACCURACY_VALUE',
'Maximum model space distance between geometric entities at asserted c
onnectivities');
#10241=UNCERTAINTY_MEASURE_WITH_UNIT(LENGTH_MEASURE(0.001),#10267,
'DISTANCE_ACCURACY_VALUE',
'Maximum model space distance between geometric entities at asserted c
onnectivities');
#10253=(
GEOMETRIC_REPRESENTATION_CONTEXT(3)
GLOBAL_UNCERTAINTY_ASSIGNED_CONTEXT((#10228))
GLOBAL_UNIT_ASSIGNED_CONTEXT((#10267,#10269,#10270))
REPRESENTATION_CONTEXT('','3D')
);
#10266=(
GEOMETRIC_REPRESENTATION_CONTEXT(3)
GLOBAL_UNCERTAINTY_ASSIGNED_CONTEXT((#10241))
GLOBAL_UNIT_ASSIGNED_CONTEXT((#10267,#10269,#10270))
REPRESENTATION_CONTEXT('','3D')
);
#10267=(
LENGTH_UNIT()
NAMED_UNIT(*)
SI_UNIT(.CENTI.,.METRE.)
);
#10269=(
NAMED_UNIT(*)
PLANE_ANGLE_UNIT()
SI_UNIT($,.RADIAN.)
);
#10270=(
NAMED_UNIT(*)
SI_UNIT($,.STERADIAN.)
SOLID_ANGLE_UNIT()
);
#10282=SHAPE_DEFINITION_REPRESENTATION(#10306,#10365);
#10306=PRODUCT_DEFINITION_SHAPE('',$,#10390);
#10365=SHAPE_REPRESENTATION('',(#5289),#10253);
#10378=PRODUCT_DEFINITION_CONTEXT('part definition',#10452,'design');
#10390=PRODUCT_DEFINITION('Upper diaphragm plate',
'Upper diaphragm plate',#10414,#10378);
#10414=PRODUCT_DEFINITION_FORMATION('',$,#10465);
#10452=APPLICATION_CONTEXT(
'Core Data for Automotive Mechanical Design Process');
#10453=PRODUCT_CONTEXT('part definition',#10452,'mechanical');
#10465=PRODUCT('Upper diaphragm plate','Upper diaphragm plate',
'Upper diaphragm plate',(#10453));
#10534=COLOUR_RGB('Sky Blue',0.24,0.69,0.87);
#10535=FILL_AREA_STYLE_COLOUR('',#10534);
#10536=FILL_AREA_STYLE('',(#10535));
#10537=SURFACE_STYLE_FILL_AREA(#10536);
#10538=SURFACE_SIDE_STYLE('',(#10537));
#10539=SURFACE_STYLE_USAGE(.BOTH.,#10538);
#10540=PRESENTATION_STYLE_ASSIGNMENT((#10539));
ENDSEC;
END-ISO-10303-21;
